ISO-10303-21;
HEADER;
FILE_DESCRIPTION (('STEP AP214'),
    '1' );
FILE_NAME ('clamping plate.step',
    '2026-10-26T19:46:16',
    ( '' ),
    ( '' ),
    'SwSTEP 2.0',
    'SolidWorks 2025',
    '' );
FILE_SCHEMA (( 'AUTOMOTIVE_DESIGN' ));
ENDSEC;

DATA;
#133=EDGE_LOOP ( 'NONE', ( #61900, #64409, #43973, #55022 ) ) ;
#267=DIRECTION ( 'NONE',  ( -0.000000000000000000, 0.000000000000000000, 1.000000000000000000 ) ) ;
#316=ORIENTED_EDGE ( 'NONE', *, *, #39996, .F. ) ;
#407=DIRECTION ( 'NONE',  ( -1.000000000000000000, -0.000000000000000000, -0.000000000000000000 ) ) ;
#592=ORIENTED_EDGE ( 'NONE', *, *, #73366, .T. ) ;
#770=DIRECTION ( 'NONE',  ( -0.000000000000000000, -0.000000000000000000, 1.000000000000000000 ) ) ;
#829=EDGE_LOOP ( 'NONE', ( #61003, #27181, #44033, #34713 ) ) ;
#973=ORIENTED_EDGE ( 'NONE', *, *, #50785, .F. ) ;
#1211=EDGE_CURVE ( 'NONE', #55047, #16735, #36653, .T. ) ;
#1286=ORIENTED_EDGE ( 'NONE', *, *, #51863, .T. ) ;
#1325=CARTESIAN_POINT ( 'NONE',  ( 38.00000000000000000, 63.00000000000000000, 15.00000000000000178 ) ) ;
#1363=VECTOR ( 'NONE', #45798, 1000.000000000000000 ) ;
#1819=VERTEX_POINT ( 'NONE', #69368 ) ;
#1915=CARTESIAN_POINT ( 'NONE',  ( 11.00000000000000000, 11.00000000000000000, -6.938893903907228378E-15 ) ) ;
#3098=DIRECTION ( 'NONE',  ( -1.000000000000000000, -0.000000000000000000, -0.000000000000000000 ) ) ;
#3234=DIRECTION ( 'NONE',  ( 0.000000000000000000, 0.000000000000000000, 1.000000000000000000 ) ) ;
#3364=DIRECTION ( 'NONE',  ( 0.000000000000000000, -6.938893903907228378E-16, -1.000000000000000000 ) ) ;
#3438=( LENGTH_UNIT ( ) NAMED_UNIT ( * ) SI_UNIT ( .MILLI., .METRE. ) );
#3439=EDGE_CURVE ( 'NONE', #16735, #46685, #67444, .T. ) ;
#3824=VERTEX_POINT ( 'NONE', #48134 ) ;
#3837=EDGE_LOOP ( 'NONE', ( #22455, #67088, #9242, #64730 ) ) ;
#4763=PRODUCT ( 'clamping plate', 'clamping plate', '', ( #67842 ) ) ;
#4914=AXIS2_PLACEMENT_3D ( 'NONE', #14307, #59975, #65633 ) ;
#4926=EDGE_LOOP ( 'NONE', ( #26254, #16119, #23664, #53536 ) ) ;
#5214=EDGE_CURVE ( 'NONE', #68280, #52559, #36027, .T. ) ;
#5416=CARTESIAN_POINT ( 'NONE',  ( -38.00000000000000000, -63.00000000000000000, 15.00000000000000178 ) ) ;
#5485=VECTOR ( 'NONE', #7412, 1000.000000000000000 ) ;
#5489=AXIS2_PLACEMENT_3D ( 'NONE', #71262, #29813, #30178 ) ;
#5601=ORIENTED_EDGE ( 'NONE', *, *, #29419, .T. ) ;
#5730=EDGE_LOOP ( 'NONE', ( #52300, #73041, #53784, #57237 ) ) ;
#5798=PLANE ( 'NONE',  #27650 ) ;
#5894=VERTEX_POINT ( 'NONE', #27771 ) ;
#6119=DIRECTION ( 'NONE',  ( -0.000000000000000000, -0.000000000000000000, 1.000000000000000000 ) ) ;
#6313=ORIENTED_EDGE ( 'NONE', *, *, #63443, .F. ) ;
#6935=PLANE ( 'NONE',  #36187 ) ;
#7023=ADVANCED_FACE ( 'NONE', ( #13651 ), #8377, .F. ) ;
#7239=CARTESIAN_POINT ( 'NONE',  ( -38.00000000000000000, 63.00000000000000000, 10.00000000000006217 ) ) ;
#7412=DIRECTION ( 'NONE',  ( -0.000000000000000000, -0.000000000000000000, 1.000000000000000000 ) ) ;
#7462=DIRECTION ( 'NONE',  ( 0.000000000000000000, -0.000000000000000000, -1.000000000000000000 ) ) ;
#7562=ORIENTED_EDGE ( 'NONE', *, *, #70963, .F. ) ;
#7697=ADVANCED_FACE ( 'NONE', ( #47169 ), #66285, .F. ) ;
#7954=EDGE_CURVE ( 'NONE', #21431, #46180, #29465, .T. ) ;
#8144=ORIENTED_EDGE ( 'NONE', *, *, #58052, .F. ) ;
#8159=VERTEX_POINT ( 'NONE', #68897 ) ;
#8348=ORIENTED_EDGE ( 'NONE', *, *, #63443, .T. ) ;
#8377=PLANE ( 'NONE',  #30265 ) ;
#9120=DIRECTION ( 'NONE',  ( 0.000000000000000000, -1.000000000000000000, 0.000000000000000000 ) ) ;
#9123=CARTESIAN_POINT ( 'NONE',  ( 38.00000000000000000, -63.00000000000000000, 15.00000000000000178 ) ) ;
#9128=LINE ( 'NONE', #27590, #55212 ) ;
#9242=ORIENTED_EDGE ( 'NONE', *, *, #34635, .F. ) ;
#9281=DIRECTION ( 'NONE',  ( 1.000000000000000000, 0.000000000000000000, 0.000000000000000000 ) ) ;
#9429=CARTESIAN_POINT ( 'NONE',  ( 38.00000000000000000, 63.00000000000000000, 15.00000000000000178 ) ) ;
#9576=EDGE_LOOP ( 'NONE', ( #41413, #25121, #17541, #36349 ) ) ;
#9793=DIRECTION ( 'NONE',  ( -1.000000000000000000, -0.000000000000000000, -0.000000000000000000 ) ) ;
#9918=ORIENTED_EDGE ( 'NONE', *, *, #73576, .F. ) ;
#10016=CARTESIAN_POINT ( 'NONE',  ( 38.00000000000000000, -53.00000000000000711, 9.999999999999991118 ) ) ;
#10028=ORIENTED_EDGE ( 'NONE', *, *, #14560, .F. ) ;
#10354=DIRECTION ( 'NONE',  ( 0.000000000000000000, 0.000000000000000000, -1.000000000000000000 ) ) ;
#10500=SHAPE_DEFINITION_REPRESENTATION ( #45734, #68567 ) ;
#10752=ADVANCED_FACE ( 'NONE', ( #67728 ), #55676, .T. ) ;
#10806=EDGE_CURVE ( 'NONE', #46685, #1819, #46395, .T. ) ;
#11021=LINE ( 'NONE', #57425, #32972 ) ;
#11130=DIRECTION ( 'NONE',  ( 0.000000000000000000, -0.000000000000000000, 1.000000000000000000 ) ) ;
#11332=DIRECTION ( 'NONE',  ( -0.000000000000000000, -6.938893903907228378E-16, 1.000000000000000000 ) ) ;
#11392=VECTOR ( 'NONE', #61265, 1000.000000000000000 ) ;
#11408=LINE ( 'NONE', #23092, #32417 ) ;
#11422=DIRECTION ( 'NONE',  ( 0.000000000000000000, 0.000000000000000000, 1.000000000000000000 ) ) ;
#11601=LINE ( 'NONE', #34637, #17538 ) ;
#12174=EDGE_LOOP ( 'NONE', ( #21258, #9918, #14434, #58629 ) ) ;
#12228=PLANE ( 'NONE',  #23634 ) ;
#12335=ORIENTED_EDGE ( 'NONE', *, *, #5214, .T. ) ;
#12351=VECTOR ( 'NONE', #20845, 1000.000000000000000 ) ;
#12524=CARTESIAN_POINT ( 'NONE',  ( 38.00000000000000000, 63.00000000000000000, 10.00000000000006217 ) ) ;
#12859=EDGE_LOOP ( 'NONE', ( #42744, #973, #13480, #10028, #55954, #61653, #66021, #74506, #56352, #42117 ) ) ;
#12860=EDGE_CURVE ( 'NONE', #50104, #70051, #38262, .T. ) ;
#13247=EDGE_CURVE ( 'NONE', #44612, #3824, #32139, .T. ) ;
#13369=LINE ( 'NONE', #71088, #36132 ) ;
#13480=ORIENTED_EDGE ( 'NONE', *, *, #51476, .F. ) ;
#13523=FACE_OUTER_BOUND ( 'NONE', #3837, .T. ) ;
#13651=FACE_OUTER_BOUND ( 'NONE', #37379, .T. ) ;
#13890=DIRECTION ( 'NONE',  ( 0.000000000000000000, 6.938893903907228378E-16, 1.000000000000000000 ) ) ;
#14007=CARTESIAN_POINT ( 'NONE',  ( -38.00000000000000000, -53.00000000000000000, 15.00000000000000178 ) ) ;
#14307=CARTESIAN_POINT ( 'NONE',  ( -38.00000000000000000, 53.00000000000000711, 9.999999999999991118 ) ) ;
#14314=DIRECTION ( 'NONE',  ( -0.000000000000000000, -0.000000000000000000, 1.000000000000000000 ) ) ;
#14371=CARTESIAN_POINT ( 'NONE',  ( 11.00000000000000000, 11.00000000000000000, -6.938893903907228378E-15 ) ) ;
#14434=ORIENTED_EDGE ( 'NONE', *, *, #21484, .F. ) ;
#14493=VECTOR ( 'NONE', #60686, 1000.000000000000000 ) ;
#14503=CIRCLE ( 'NONE', #4914, 9.999999999999998224 ) ;
#14507=ORIENTED_EDGE ( 'NONE', *, *, #14560, .T. ) ;
#14560=EDGE_CURVE ( 'NONE', #5894, #64638, #14503, .T. ) ;
#14627=VECTOR ( 'NONE', #34133, 1000.000000000000000 ) ;
#14731=( LENGTH_UNIT ( ) NAMED_UNIT ( * ) SI_UNIT ( .MILLI., .METRE. ) );
#14771=CARTESIAN_POINT ( 'NONE',  ( -11.00000000000000000, 11.00000000000000000, 25.00000000000000000 ) ) ;
#15047=MECHANICAL_DESIGN_GEOMETRIC_PRESENTATION_REPRESENTATION('',(#23520),#39195);
#15194=ORIENTED_EDGE ( 'NONE', *, *, #24961, .T. ) ;
#15283=DIRECTION ( 'NONE',  ( -0.000000000000000000, -1.000000000000000000, -0.000000000000000000 ) ) ;
#15581=ADVANCED_BREP_SHAPE_REPRESENTATION ( '', ( #67429, #57354 ), #40540 ) ;
#15742=DIRECTION ( 'NONE',  ( 1.577021341797097560E-16, -1.000000000000000000, 0.000000000000000000 ) ) ;
#15765=ADVANCED_FACE ( 'NONE', ( #50802 ), #33852, .T. ) ;
#15803=CARTESIAN_POINT ( 'NONE',  ( 38.00000000000000000, 53.00000000000000711, 9.999999999999991118 ) ) ;
#15947=VECTOR ( 'NONE', #6119, 1000.000000000000000 ) ;
#16119=ORIENTED_EDGE ( 'NONE', *, *, #16438, .F. ) ;
#16247=DIRECTION ( 'NONE',  ( 0.000000000000000000, -1.000000000000000000, -6.938893903907228378E-16 ) ) ;
#16438=EDGE_CURVE ( 'NONE', #71834, #46180, #74470, .T. ) ;
#16735=VERTEX_POINT ( 'NONE', #26485 ) ;
#16739=CARTESIAN_POINT ( 'NONE',  ( 38.00000000000000000, -52.99999999999999289, 25.00000000000000000 ) ) ;
#16780=VECTOR ( 'NONE', #3098, 1000.000000000000000 ) ;
#16978=CARTESIAN_POINT ( 'NONE',  ( 38.00000000000000000, 52.99999999999999289, 25.00000000000000000 ) ) ;
#17359=ORIENTED_EDGE ( 'NONE', *, *, #49692, .T. ) ;
#17428=DIRECTION ( 'NONE',  ( -0.000000000000000000, 1.000000000000000000, -0.000000000000000000 ) ) ;
#17494=ADVANCED_FACE ( 'NONE', ( #28450 ), #74469, .F. ) ;
#17538=VECTOR ( 'NONE', #57643, 1000.000000000000000 ) ;
#17541=ORIENTED_EDGE ( 'NONE', *, *, #5214, .F. ) ;
#17571=EDGE_CURVE ( 'NONE', #40096, #21431, #73726, .T. ) ;
#17666=CARTESIAN_POINT ( 'NONE',  ( 11.00000000000000355, -11.00000000000000000, 25.00000000000000000 ) ) ;
#17796=LINE ( 'NONE', #57812, #53346 ) ;
#17908=UNCERTAINTY_MEASURE_WITH_UNIT (LENGTH_MEASURE( 1.000000000000000082E-05 ), #14731, 'distance_accuracy_value', 'NONE');
#17946=CARTESIAN_POINT ( 'NONE',  ( 11.00000000000000000, 11.00000000000000000, 25.00000000000000000 ) ) ;
#17988=CARTESIAN_POINT ( 'NONE',  ( 11.00000000000000000, 11.00000000000000000, -6.938893903907228378E-15 ) ) ;
#18123=VECTOR ( 'NONE', #11332, 1000.000000000000000 ) ;
#18181=CARTESIAN_POINT ( 'NONE',  ( 38.00000000000000000, 52.99999999999992895, -6.791607979884335933E-15 ) ) ;
#18407=DIRECTION ( 'NONE',  ( 0.000000000000000000, -1.000000000000000000, 0.000000000000000000 ) ) ;
#18482=UNCERTAINTY_MEASURE_WITH_UNIT (LENGTH_MEASURE( 1.000000000000000082E-05 ), #3438, 'distance_accuracy_value', 'NONE');
#18525=PLANE ( 'NONE',  #57791 ) ;
#19211=ORIENTED_EDGE ( 'NONE', *, *, #70963, .T. ) ;
#19664=VERTEX_POINT ( 'NONE', #66373 ) ;
#19712=ADVANCED_FACE ( 'NONE', ( #73162 ), #27500, .T. ) ;
#19828=CARTESIAN_POINT ( 'NONE',  ( 38.00000000000000000, -53.00000000000000000, 15.00000000000000178 ) ) ;
#20341=ORIENTED_EDGE ( 'NONE', *, *, #62277, .T. ) ;
#20705=LINE ( 'NONE', #72392, #29944 ) ;
#20845=DIRECTION ( 'NONE',  ( 0.000000000000000000, -1.000000000000000000, 0.000000000000000000 ) ) ;
#21258=ORIENTED_EDGE ( 'NONE', *, *, #39996, .T. ) ;
#21431=VERTEX_POINT ( 'NONE', #54015 ) ;
#21484=EDGE_CURVE ( 'NONE', #24322, #55047, #37031, .T. ) ;
#21501=CARTESIAN_POINT ( 'NONE',  ( -38.00000000000000000, -53.00000000000000000, 15.00000000000000178 ) ) ;
#21664=DIRECTION ( 'NONE',  ( -0.000000000000000000, 0.000000000000000000, 1.000000000000000000 ) ) ;
#21749=ORIENTED_EDGE ( 'NONE', *, *, #32302, .T. ) ;
#21756=DIRECTION ( 'NONE',  ( -0.000000000000000000, 0.000000000000000000, 1.000000000000000000 ) ) ;
#21936=CARTESIAN_POINT ( 'NONE',  ( 11.00000000000000355, -11.00000000000000000, -6.938893903907228378E-15 ) ) ;
#22030=PLANE ( 'NONE',  #43320 ) ;
#22036=CARTESIAN_POINT ( 'NONE',  ( -38.00000000000000000, 52.99999999999999289, 25.00000000000000000 ) ) ;
#22075=CARTESIAN_POINT ( 'NONE',  ( -38.00000000000000000, -53.00000000000000711, 9.999999999999991118 ) ) ;
#22376=FACE_OUTER_BOUND ( 'NONE', #48684, .T. ) ;
#22455=ORIENTED_EDGE ( 'NONE', *, *, #33476, .T. ) ;
#22490=CARTESIAN_POINT ( 'NONE',  ( -38.00000000000000000, 53.00000000000000711, 9.999999999999991118 ) ) ;
#22776=DIRECTION ( 'NONE',  ( -1.000000000000000000, 0.000000000000000000, -0.000000000000000000 ) ) ;
#23092=CARTESIAN_POINT ( 'NONE',  ( 38.00000000000000000, 52.99999999999992895, -6.791607979884335933E-15 ) ) ;
#23329=LINE ( 'NONE', #73897, #54006 ) ;
#23362=EDGE_CURVE ( 'NONE', #37342, #50104, #25702, .T. ) ;
#23520=STYLED_ITEM('',(#74713),#67429);
#23549=FACE_OUTER_BOUND ( 'NONE', #49280, .T. ) ;
#23570=CIRCLE ( 'NONE', #54936, 9.999999999999996447 ) ;
#23587=LINE ( 'NONE', #29627, #61915 ) ;
#23600=LINE ( 'NONE', #17946, #47805 ) ;
#23634=AXIS2_PLACEMENT_3D ( 'NONE', #29588, #52601, #11130 ) ;
#23649=LINE ( 'NONE', #17988, #5485 ) ;
#23664=ORIENTED_EDGE ( 'NONE', *, *, #51863, .F. ) ;
#24188=VERTEX_POINT ( 'NONE', #32540 ) ;
#24273=FACE_OUTER_BOUND ( 'NONE', #4926, .T. ) ;
#24289=VECTOR ( 'NONE', #41156, 1000.000000000000000 ) ;
#24322=VERTEX_POINT ( 'NONE', #21936 ) ;
#24472=VECTOR ( 'NONE', #15283, 1000.000000000000000 ) ;
#24567=VERTEX_POINT ( 'NONE', #29100 ) ;
#24938=VECTOR ( 'NONE', #9120, 1000.000000000000000 ) ;
#24961=EDGE_CURVE ( 'NONE', #38816, #68280, #66008, .T. ) ;
#25121=ORIENTED_EDGE ( 'NONE', *, *, #67516, .F. ) ;
#25455=AXIS2_PLACEMENT_3D ( 'NONE', #58514, #42891, #66659 ) ;
#25471=CARTESIAN_POINT ( 'NONE',  ( -38.00000000000000000, -63.00000000000000000, 15.00000000000000178 ) ) ;
#25678=CARTESIAN_POINT ( 'NONE',  ( -11.00000000000000000, 11.00000000000000000, -6.938893903907228378E-15 ) ) ;
#25702=LINE ( 'NONE', #14007, #24938 ) ;
#26254=ORIENTED_EDGE ( 'NONE', *, *, #7954, .T. ) ;
#26485=CARTESIAN_POINT ( 'NONE',  ( -10.99999999999999645, 11.00000000000000355, -6.791607979884335933E-15 ) ) ;
#26877=EDGE_CURVE ( 'NONE', #34844, #24188, #11408, .T. ) ;
#26880=LINE ( 'NONE', #72539, #12351 ) ;
#26990=EDGE_CURVE ( 'NONE', #24188, #5894, #35909, .T. ) ;
#27023=VERTEX_POINT ( 'NONE', #29506 ) ;
#27181=ORIENTED_EDGE ( 'NONE', *, *, #26990, .F. ) ;
#27482=CARTESIAN_POINT ( 'NONE',  ( 38.00000000000000000, -53.00000000000000711, -5.204170427930421283E-15 ) ) ;
#27500=CYLINDRICAL_SURFACE ( 'NONE', #58119, 9.999999999999998224 ) ;
#27582=DIRECTION ( 'NONE',  ( 0.000000000000000000, 6.938893903907228378E-16, -1.000000000000000000 ) ) ;
#27590=CARTESIAN_POINT ( 'NONE',  ( 38.00000000000000000, -53.00000000000000711, -5.204170427930421283E-15 ) ) ;
#27650=AXIS2_PLACEMENT_3D ( 'NONE', #45042, #27679, #62376 ) ;
#27679=DIRECTION ( 'NONE',  ( -0.000000000000000000, 1.000000000000000000, 0.000000000000000000 ) ) ;
#27771=CARTESIAN_POINT ( 'NONE',  ( -38.00000000000000000, 52.99999999999992895, -6.791607979884335933E-15 ) ) ;
#27921=EDGE_LOOP ( 'NONE', ( #39612, #60180, #46406, #21749 ) ) ;
#27958=APPLICATION_CONTEXT ( 'automotive_design' ) ;
#28004=DIRECTION ( 'NONE',  ( -0.000000000000000000, -1.000000000000000000, -0.000000000000000000 ) ) ;
#28204=PRODUCT_DEFINITION_CONTEXT ( 'detailed design', #27958, 'design' ) ;
#28313=ORIENTED_EDGE ( 'NONE', *, *, #58467, .F. ) ;
#28358=CARTESIAN_POINT ( 'NONE',  ( 11.00000000000000000, 11.00000000000000000, -6.938893903907228378E-15 ) ) ;
#28450=FACE_OUTER_BOUND ( 'NONE', #41918, .T. ) ;
#28674=VECTOR ( 'NONE', #14314, 1000.000000000000000 ) ;
#28776=DIRECTION ( 'NONE',  ( 1.000000000000000000, 0.000000000000000000, 0.000000000000000000 ) ) ;
#28788=CARTESIAN_POINT ( 'NONE',  ( -10.99999999999999645, -11.00000000000000000, -6.938893903907228378E-15 ) ) ;
#29051=LINE ( 'NONE', #52071, #31360 ) ;
#29100=CARTESIAN_POINT ( 'NONE',  ( -38.00000000000000000, 63.00000000000000000, 15.00000000000000178 ) ) ;
#29123=LINE ( 'NONE', #34805, #15947 ) ;
#29210=DIRECTION ( 'NONE',  ( -1.000000000000000000, 0.000000000000000000, -0.000000000000000000 ) ) ;
#29272=DIRECTION ( 'NONE',  ( -1.577021341797097560E-16, 1.000000000000000000, -0.000000000000000000 ) ) ;
#29419=EDGE_CURVE ( 'NONE', #45526, #41123, #13369, .T. ) ;
#29465=LINE ( 'NONE', #52475, #24289 ) ;
#29506=CARTESIAN_POINT ( 'NONE',  ( 38.00000000000000000, -53.00000000000000000, 15.00000000000000178 ) ) ;
#29588=CARTESIAN_POINT ( 'NONE',  ( 38.00000000000000000, -63.00000000000000000, 15.00000000000000178 ) ) ;
#29627=CARTESIAN_POINT ( 'NONE',  ( 38.00000000000000000, -63.00000000000000000, 10.00000000000006217 ) ) ;
#29652=ORIENTED_EDGE ( 'NONE', *, *, #26990, .T. ) ;
#29744=ORIENTED_EDGE ( 'NONE', *, *, #34635, .T. ) ;
#29813=DIRECTION ( 'NONE',  ( 0.000000000000000000, -1.000000000000000000, 0.000000000000000000 ) ) ;
#29944=VECTOR ( 'NONE', #3364, 1000.000000000000000 ) ;
#30178=DIRECTION ( 'NONE',  ( 0.000000000000000000, -0.000000000000000000, -1.000000000000000000 ) ) ;
#30265=AXIS2_PLACEMENT_3D ( 'NONE', #31393, #52934, #47257 ) ;
#30298=ADVANCED_FACE ( 'NONE', ( #43936 ), #22030, .F. ) ;
#30468=CARTESIAN_POINT ( 'NONE',  ( -38.00000000000000000, -63.00000000000000000, 10.00000000000006217 ) ) ;
#30773=ORIENTED_EDGE ( 'NONE', *, *, #1211, .T. ) ;
#30911=FACE_OUTER_BOUND ( 'NONE', #55593, .T. ) ;
#30993=DIRECTION ( 'NONE',  ( -1.577021341797097560E-16, 1.000000000000000000, -0.000000000000000000 ) ) ;
#31262=ORIENTED_EDGE ( 'NONE', *, *, #58223, .F. ) ;
#31358=( NAMED_UNIT ( * ) SI_UNIT ( $, .STERADIAN. ) SOLID_ANGLE_UNIT ( ) );
#31360=VECTOR ( 'NONE', #407, 1000.000000000000000 ) ;
#31393=CARTESIAN_POINT ( 'NONE',  ( -11.00000000000000000, 11.00000000000000000, -6.938893903907228378E-15 ) ) ;
#31562=ADVANCED_FACE ( 'NONE', ( #58627, #24273 ), #6935, .F. ) ;
#32139=LINE ( 'NONE', #9123, #70461 ) ;
#32297=ORIENTED_EDGE ( 'NONE', *, *, #13247, .T. ) ;
#32302=EDGE_CURVE ( 'NONE', #27023, #37342, #71877, .T. ) ;
#32417=VECTOR ( 'NONE', #17428, 1000.000000000000000 ) ;
#32540=CARTESIAN_POINT ( 'NONE',  ( 38.00000000000000000, 52.99999999999992895, -6.791607979884335933E-15 ) ) ;
#32608=EDGE_CURVE ( 'NONE', #8159, #21431, #37429, .T. ) ;
#32754=CARTESIAN_POINT ( 'NONE',  ( 38.00000000000000000, -53.00000000000000711, 9.999999999999991118 ) ) ;
#32803=EDGE_CURVE ( 'NONE', #34844, #19664, #9128, .T. ) ;
#32972=VECTOR ( 'NONE', #72625, 1000.000000000000000 ) ;
#33047=DIRECTION ( 'NONE',  ( -1.000000000000000000, -0.000000000000000000, -0.000000000000000000 ) ) ;
#33048=PRODUCT_DEFINITION ( 'UNKNOWN', '', #50215, #28204 ) ;
#33386=VECTOR ( 'NONE', #30993, 1000.000000000000000 ) ;
#33476=EDGE_CURVE ( 'NONE', #46180, #37342, #58803, .T. ) ;
#33563=DIRECTION ( 'NONE',  ( 0.000000000000000000, 0.000000000000000000, 1.000000000000000000 ) ) ;
#33566=ORIENTED_EDGE ( 'NONE', *, *, #73576, .T. ) ;
#33852=PLANE ( 'NONE',  #33890 ) ;
#33862=CARTESIAN_POINT ( 'NONE',  ( 38.00000000000000000, -63.00000000000000000, 15.00000000000000178 ) ) ;
#33890=AXIS2_PLACEMENT_3D ( 'NONE', #22490, #63234, #267 ) ;
#34133=DIRECTION ( 'NONE',  ( -1.000000000000000000, -0.000000000000000000, -0.000000000000000000 ) ) ;
#34459=DIRECTION ( 'NONE',  ( 1.000000000000000000, 0.000000000000000000, 0.000000000000000000 ) ) ;
#34635=EDGE_CURVE ( 'NONE', #71834, #27023, #20705, .T. ) ;
#34637=CARTESIAN_POINT ( 'NONE',  ( -38.00000000000000000, 52.99999999999992895, -6.791607979884335933E-15 ) ) ;
#34713=ORIENTED_EDGE ( 'NONE', *, *, #32803, .T. ) ;
#34805=CARTESIAN_POINT ( 'NONE',  ( -11.00000000000000000, 11.00000000000000000, -6.938893903907228378E-15 ) ) ;
#34844=VERTEX_POINT ( 'NONE', #27482 ) ;
#35028=ORIENTED_EDGE ( 'NONE', *, *, #10806, .T. ) ;
#35203=DIRECTION ( 'NONE',  ( 0.000000000000000000, 0.000000000000000000, 1.000000000000000000 ) ) ;
#35909=LINE ( 'NONE', #18181, #60128 ) ;
#36027=LINE ( 'NONE', #47332, #38590 ) ;
#36116=APPLICATION_CONTEXT ( 'automotive_design' ) ;
#36132=VECTOR ( 'NONE', #59787, 1000.000000000000000 ) ;
#36187=AXIS2_PLACEMENT_3D ( 'NONE', #52960, #69569, #29210 ) ;
#36349=ORIENTED_EDGE ( 'NONE', *, *, #64128, .T. ) ;
#36368=CARTESIAN_POINT ( 'NONE',  ( 38.00000000000000000, 63.00000000000000000, 15.00000000000000178 ) ) ;
#36410=CARTESIAN_POINT ( 'NONE',  ( -38.00000000000000000, 53.00000000000000000, 15.00000000000000178 ) ) ;
#36500=FACE_OUTER_BOUND ( 'NONE', #133, .T. ) ;
#36561=PLANE ( 'NONE',  #60737 ) ;
#36653=LINE ( 'NONE', #25678, #66518 ) ;
#37031=LINE ( 'NONE', #14371, #33386 ) ;
#37303=ORIENTED_EDGE ( 'NONE', *, *, #50900, .T. ) ;
#37342=VERTEX_POINT ( 'NONE', #21501 ) ;
#37379=EDGE_LOOP ( 'NONE', ( #19211, #64693, #38681, #37303 ) ) ;
#37429=LINE ( 'NONE', #59334, #16780 ) ;
#37809=DIRECTION ( 'NONE',  ( 1.577021341797097560E-16, -1.000000000000000000, 0.000000000000000000 ) ) ;
#38018=CIRCLE ( 'NONE', #59707, 9.999999999999996447 ) ;
#38262=LINE ( 'NONE', #5416, #11392 ) ;
#38397=CARTESIAN_POINT ( 'NONE',  ( 38.00000000000000000, -63.00000000000000000, 15.00000000000000178 ) ) ;
#38590=VECTOR ( 'NONE', #65421, 1000.000000000000000 ) ;
#38681=ORIENTED_EDGE ( 'NONE', *, *, #3439, .F. ) ;
#38774=LINE ( 'NONE', #38397, #55677 ) ;
#38806=CARTESIAN_POINT ( 'NONE',  ( 11.00000000000000355, -11.00000000000000000, -6.938893903907228378E-15 ) ) ;
#38816=VERTEX_POINT ( 'NONE', #12524 ) ;
#38905=VECTOR ( 'NONE', #68933, 1000.000000000000000 ) ;
#39028=ORIENTED_EDGE ( 'NONE', *, *, #62277, .F. ) ;
#39144=DIRECTION ( 'NONE',  ( 0.000000000000000000, 0.000000000000000000, -1.000000000000000000 ) ) ;
#39195=( GEOMETRIC_REPRESENTATION_CONTEXT ( 3 ) GLOBAL_UNCERTAINTY_ASSIGNED_CONTEXT ( ( #17908 ) ) GLOBAL_UNIT_ASSIGNED_CONTEXT ( ( #14731, #49063, #42663 ) ) REPRESENTATION_CONTEXT ( 'NONE', 'WORKASPACE' ) );
#39430=CARTESIAN_POINT ( 'NONE',  ( 38.00000000000000000, -52.99999999999999289, 25.00000000000000000 ) ) ;
#39612=ORIENTED_EDGE ( 'NONE', *, *, #23362, .T. ) ;
#39618=EDGE_LOOP ( 'NONE', ( #62154, #52713, #57535, #8348 ) ) ;
#39996=EDGE_CURVE ( 'NONE', #60275, #45526, #23600, .T. ) ;
#40096=VERTEX_POINT ( 'NONE', #36410 ) ;
#40540=( GEOMETRIC_REPRESENTATION_CONTEXT ( 3 ) GLOBAL_UNCERTAINTY_ASSIGNED_CONTEXT ( ( #18482 ) ) GLOBAL_UNIT_ASSIGNED_CONTEXT ( ( #3438, #61150, #31358 ) ) REPRESENTATION_CONTEXT ( 'NONE', 'WORKASPACE' ) );
#40950=DIRECTION ( 'NONE',  ( -1.000000000000000000, -0.000000000000000000, -0.000000000000000000 ) ) ;
#41123=VERTEX_POINT ( 'NONE', #74359 ) ;
#41156=DIRECTION ( 'NONE',  ( -0.000000000000000000, -1.000000000000000000, -0.000000000000000000 ) ) ;
#41170=FACE_OUTER_BOUND ( 'NONE', #12174, .T. ) ;
#41413=ORIENTED_EDGE ( 'NONE', *, *, #50785, .T. ) ;
#41422=CARTESIAN_POINT ( 'NONE',  ( 38.00000000000000000, 63.00000000000000000, 15.00000000000000178 ) ) ;
#41918=EDGE_LOOP ( 'NONE', ( #73292, #1286, #29744, #44083, #32297, #592, #41983, #45997, #15194, #12335 ) ) ;
#41983=ORIENTED_EDGE ( 'NONE', *, *, #26877, .T. ) ;
#42117=ORIENTED_EDGE ( 'NONE', *, *, #7954, .F. ) ;
#42521=ADVANCED_FACE ( 'NONE', ( #50969 ), #46427, .F. ) ;
#42634=VECTOR ( 'NONE', #71050, 1000.000000000000000 ) ;
#42663=( NAMED_UNIT ( * ) SI_UNIT ( $, .STERADIAN. ) SOLID_ANGLE_UNIT ( ) );
#42744=ORIENTED_EDGE ( 'NONE', *, *, #17571, .F. ) ;
#42891=DIRECTION ( 'NONE',  ( 0.000000000000000000, 0.000000000000000000, -1.000000000000000000 ) ) ;
#43219=EDGE_CURVE ( 'NONE', #1819, #60275, #23329, .T. ) ;
#43320=AXIS2_PLACEMENT_3D ( 'NONE', #44683, #10354, #61664 ) ;
#43936=FACE_OUTER_BOUND ( 'NONE', #27921, .T. ) ;
#43973=ORIENTED_EDGE ( 'NONE', *, *, #24961, .F. ) ;
#44033=ORIENTED_EDGE ( 'NONE', *, *, #26877, .F. ) ;
#44083=ORIENTED_EDGE ( 'NONE', *, *, #50533, .T. ) ;
#44612=VERTEX_POINT ( 'NONE', #33862 ) ;
#44683=CARTESIAN_POINT ( 'NONE',  ( 38.00000000000000000, -53.00000000000000000, 15.00000000000000178 ) ) ;
#44956=DIRECTION ( 'NONE',  ( -1.000000000000000000, -0.000000000000000000, -0.000000000000000000 ) ) ;
#45042=CARTESIAN_POINT ( 'NONE',  ( -11.00000000000000000, 11.00000000000000000, -6.938893903907228378E-15 ) ) ;
#45526=VERTEX_POINT ( 'NONE', #67900 ) ;
#45734=PRODUCT_DEFINITION_SHAPE ( 'NONE', 'NONE',  #33048 ) ;
#45798=DIRECTION ( 'NONE',  ( -0.000000000000000000, -6.938893903907228378E-16, 1.000000000000000000 ) ) ;
#45997=ORIENTED_EDGE ( 'NONE', *, *, #58467, .T. ) ;
#46180=VERTEX_POINT ( 'NONE', #73102 ) ;
#46395=LINE ( 'NONE', #47494, #67987 ) ;
#46406=ORIENTED_EDGE ( 'NONE', *, *, #50533, .F. ) ;
#46427=PLANE ( 'NONE',  #73302 ) ;
#46664=LINE ( 'NONE', #64024, #38905 ) ;
#46685=VERTEX_POINT ( 'NONE', #28788 ) ;
#46763=LINE ( 'NONE', #16978, #18123 ) ;
#46781=PLANE ( 'NONE',  #5489 ) ;
#47064=PLANE ( 'NONE',  #50118 ) ;
#47169=FACE_OUTER_BOUND ( 'NONE', #9576, .T. ) ;
#47257=DIRECTION ( 'NONE',  ( 1.577021341797097560E-16, -1.000000000000000000, 0.000000000000000000 ) ) ;
#47290=VECTOR ( 'NONE', #15742, 1000.000000000000000 ) ;
#47332=CARTESIAN_POINT ( 'NONE',  ( 38.00000000000000000, 53.00000000000000000, 15.00000000000000178 ) ) ;
#47494=CARTESIAN_POINT ( 'NONE',  ( -10.99999999999999645, -11.00000000000000000, -6.938893903907228378E-15 ) ) ;
#47805=VECTOR ( 'NONE', #29272, 1000.000000000000000 ) ;
#47919=DIRECTION ( 'NONE',  ( -1.577021341797097560E-16, 1.000000000000000000, 0.000000000000000000 ) ) ;
#48134=CARTESIAN_POINT ( 'NONE',  ( 38.00000000000000000, -63.00000000000000000, 10.00000000000006217 ) ) ;
#48684=EDGE_LOOP ( 'NONE', ( #5601, #58189, #52494, #33566 ) ) ;
#49063=( NAMED_UNIT ( * ) PLANE_ANGLE_UNIT ( ) SI_UNIT ( $, .RADIAN. ) );
#49280=EDGE_LOOP ( 'NONE', ( #56244, #6313, #63621, #17359 ) ) ;
#49692=EDGE_CURVE ( 'NONE', #44612, #50104, #38774, .T. ) ;
#50104=VERTEX_POINT ( 'NONE', #25471 ) ;
#50118=AXIS2_PLACEMENT_3D ( 'NONE', #41422, #18407, #7462 ) ;
#50215=PRODUCT_DEFINITION_FORMATION_WITH_SPECIFIED_SOURCE ( 'ANY', '', #4763, .NOT_KNOWN. ) ;
#50226=DIRECTION ( 'NONE',  ( 0.000000000000000000, 0.000000000000000000, -1.000000000000000000 ) ) ;
#50533=EDGE_CURVE ( 'NONE', #27023, #44612, #26880, .T. ) ;
#50653=EDGE_LOOP ( 'NONE', ( #14507, #8144, #28313, #29652 ) ) ;
#50785=EDGE_CURVE ( 'NONE', #24567, #40096, #17796, .T. ) ;
#50802=FACE_OUTER_BOUND ( 'NONE', #12859, .T. ) ;
#50808=CARTESIAN_POINT ( 'NONE',  ( 38.00000000000000000, 52.99999999999992895, -6.791607979884335933E-15 ) ) ;
#50900=EDGE_CURVE ( 'NONE', #16735, #41123, #29123, .T. ) ;
#50969=FACE_OUTER_BOUND ( 'NONE', #5730, .T. ) ;
#51476=EDGE_CURVE ( 'NONE', #64638, #24567, #46664, .T. ) ;
#51713=CARTESIAN_POINT ( 'NONE',  ( 38.00000000000000000, 52.99999999999999289, 25.00000000000000000 ) ) ;
#51863=EDGE_CURVE ( 'NONE', #8159, #71834, #62063, .T. ) ;
#52071=CARTESIAN_POINT ( 'NONE',  ( 38.00000000000000000, 63.00000000000000000, 10.00000000000006217 ) ) ;
#52300=ORIENTED_EDGE ( 'NONE', *, *, #17571, .T. ) ;
#52475=CARTESIAN_POINT ( 'NONE',  ( -38.00000000000000000, -52.99999999999999289, 25.00000000000000000 ) ) ;
#52494=ORIENTED_EDGE ( 'NONE', *, *, #1211, .F. ) ;
#52559=VERTEX_POINT ( 'NONE', #72552 ) ;
#52601=DIRECTION ( 'NONE',  ( -0.000000000000000000, 1.000000000000000000, 0.000000000000000000 ) ) ;
#52713=ORIENTED_EDGE ( 'NONE', *, *, #32803, .F. ) ;
#52860=DIRECTION ( 'NONE',  ( 1.000000000000000000, 1.577021341797097560E-16, 0.000000000000000000 ) ) ;
#52934=DIRECTION ( 'NONE',  ( -1.000000000000000000, -1.577021341797097560E-16, 0.000000000000000000 ) ) ;
#52960=CARTESIAN_POINT ( 'NONE',  ( 38.00000000000000000, -52.99999999999999289, 25.00000000000000000 ) ) ;
#53346=VECTOR ( 'NONE', #28004, 1000.000000000000000 ) ;
#53536=ORIENTED_EDGE ( 'NONE', *, *, #32608, .T. ) ;
#53633=CARTESIAN_POINT ( 'NONE',  ( 38.00000000000000000, 53.00000000000000000, 15.00000000000000178 ) ) ;
#53784=ORIENTED_EDGE ( 'NONE', *, *, #57898, .F. ) ;
#54001=ORIENTED_EDGE ( 'NONE', *, *, #21484, .T. ) ;
#54006=VECTOR ( 'NONE', #74267, 1000.000000000000000 ) ;
#54015=CARTESIAN_POINT ( 'NONE',  ( -38.00000000000000000, 52.99999999999999289, 25.00000000000000000 ) ) ;
#54389=AXIS2_PLACEMENT_3D ( 'NONE', #73360, #22776, #21664 ) ;
#54936=AXIS2_PLACEMENT_3D ( 'NONE', #22075, #9281, #61712 ) ;
#54979=ADVANCED_FACE ( 'NONE', ( #22376 ), #5798, .F. ) ;
#55022=ORIENTED_EDGE ( 'NONE', *, *, #58052, .T. ) ;
#55047=VERTEX_POINT ( 'NONE', #28358 ) ;
#55212=VECTOR ( 'NONE', #44956, 1000.000000000000000 ) ;
#55414=ADVANCED_FACE ( 'NONE', ( #41170 ), #18525, .F. ) ;
#55509=CIRCLE ( 'NONE', #65126, 9.999999999999998224 ) ;
#55593=EDGE_LOOP ( 'NONE', ( #66347, #31262, #39028, #35028 ) ) ;
#55676=CYLINDRICAL_SURFACE ( 'NONE', #57113, 9.999999999999998224 ) ;
#55677=VECTOR ( 'NONE', #56498, 1000.000000000000000 ) ;
#55744=FACE_OUTER_BOUND ( 'NONE', #829, .T. ) ;
#55954=ORIENTED_EDGE ( 'NONE', *, *, #67737, .F. ) ;
#56244=ORIENTED_EDGE ( 'NONE', *, *, #12860, .T. ) ;
#56352=ORIENTED_EDGE ( 'NONE', *, *, #33476, .F. ) ;
#56498=DIRECTION ( 'NONE',  ( -1.000000000000000000, -0.000000000000000000, -0.000000000000000000 ) ) ;
#57113=AXIS2_PLACEMENT_3D ( 'NONE', #10016, #33047, #3234 ) ;
#57237=ORIENTED_EDGE ( 'NONE', *, *, #67516, .T. ) ;
#57261=VECTOR ( 'NONE', #70965, 1000.000000000000000 ) ;
#57354=AXIS2_PLACEMENT_3D ( 'NONE', #63097, #11422, #34459 ) ;
#57425=CARTESIAN_POINT ( 'NONE',  ( -10.99999999999999645, -11.00000000000000000, -6.938893903907228378E-15 ) ) ;
#57535=ORIENTED_EDGE ( 'NONE', *, *, #73366, .F. ) ;
#57643=DIRECTION ( 'NONE',  ( -0.000000000000000000, 1.000000000000000000, -0.000000000000000000 ) ) ;
#57791=AXIS2_PLACEMENT_3D ( 'NONE', #1915, #52860, #47919 ) ;
#57812=CARTESIAN_POINT ( 'NONE',  ( -38.00000000000000000, 53.00000000000000000, 15.00000000000000178 ) ) ;
#57898=EDGE_CURVE ( 'NONE', #52559, #8159, #46763, .T. ) ;
#58052=EDGE_CURVE ( 'NONE', #38816, #64638, #29051, .T. ) ;
#58119=AXIS2_PLACEMENT_3D ( 'NONE', #15803, #9793, #33563 ) ;
#58189=ORIENTED_EDGE ( 'NONE', *, *, #50900, .F. ) ;
#58220=CARTESIAN_POINT ( 'NONE',  ( 38.00000000000000000, 53.00000000000000711, 9.999999999999991118 ) ) ;
#58223=EDGE_CURVE ( 'NONE', #24322, #60275, #59214, .T. ) ;
#58440=VECTOR ( 'NONE', #37809, 1000.000000000000000 ) ;
#58467=EDGE_CURVE ( 'NONE', #24188, #38816, #55509, .T. ) ;
#58514=CARTESIAN_POINT ( 'NONE',  ( 38.00000000000000000, 53.00000000000000000, 15.00000000000000178 ) ) ;
#58627=FACE_BOUND ( 'NONE', #62732, .T. ) ;
#58629=ORIENTED_EDGE ( 'NONE', *, *, #58223, .T. ) ;
#58803=LINE ( 'NONE', #70848, #62407 ) ;
#59214=LINE ( 'NONE', #38806, #14493 ) ;
#59334=CARTESIAN_POINT ( 'NONE',  ( 38.00000000000000000, 52.99999999999999289, 25.00000000000000000 ) ) ;
#59575=CARTESIAN_POINT ( 'NONE',  ( 38.00000000000000000, -52.99999999999999289, 25.00000000000000000 ) ) ;
#59663=DIRECTION ( 'NONE',  ( -1.000000000000000000, -0.000000000000000000, -0.000000000000000000 ) ) ;
#59707=AXIS2_PLACEMENT_3D ( 'NONE', #32754, #68554, #39144 ) ;
#59787=DIRECTION ( 'NONE',  ( -1.000000000000000000, -0.000000000000000000, -0.000000000000000000 ) ) ;
#59975=DIRECTION ( 'NONE',  ( 1.000000000000000000, 0.000000000000000000, 0.000000000000000000 ) ) ;
#60128=VECTOR ( 'NONE', #69496, 1000.000000000000000 ) ;
#60180=ORIENTED_EDGE ( 'NONE', *, *, #49692, .F. ) ;
#60275=VERTEX_POINT ( 'NONE', #17666 ) ;
#60686=DIRECTION ( 'NONE',  ( -0.000000000000000000, -0.000000000000000000, 1.000000000000000000 ) ) ;
#60737=AXIS2_PLACEMENT_3D ( 'NONE', #59575, #65593, #13890 ) ;
#60779=ORIENTED_EDGE ( 'NONE', *, *, #43219, .F. ) ;
#61003=ORIENTED_EDGE ( 'NONE', *, *, #67737, .T. ) ;
#61150=( NAMED_UNIT ( * ) PLANE_ANGLE_UNIT ( ) SI_UNIT ( $, .RADIAN. ) );
#61265=DIRECTION ( 'NONE',  ( 0.000000000000000000, 0.000000000000000000, -1.000000000000000000 ) ) ;
#61388=DIRECTION ( 'NONE',  ( 1.000000000000000000, 0.000000000000000000, 0.000000000000000000 ) ) ;
#61653=ORIENTED_EDGE ( 'NONE', *, *, #67950, .F. ) ;
#61664=DIRECTION ( 'NONE',  ( -1.000000000000000000, 0.000000000000000000, -0.000000000000000000 ) ) ;
#61712=DIRECTION ( 'NONE',  ( 0.000000000000000000, 0.000000000000000000, -1.000000000000000000 ) ) ;
#61900=ORIENTED_EDGE ( 'NONE', *, *, #51476, .T. ) ;
#61915=VECTOR ( 'NONE', #40950, 1000.000000000000000 ) ;
#62063=LINE ( 'NONE', #39430, #24472 ) ;
#62154=ORIENTED_EDGE ( 'NONE', *, *, #67950, .T. ) ;
#62277=EDGE_CURVE ( 'NONE', #46685, #24322, #11021, .T. ) ;
#62376=DIRECTION ( 'NONE',  ( 0.000000000000000000, -0.000000000000000000, 1.000000000000000000 ) ) ;
#62407=VECTOR ( 'NONE', #64084, 1000.000000000000000 ) ;
#62732=EDGE_LOOP ( 'NONE', ( #72639, #316, #60779, #7562 ) ) ;
#63097=CARTESIAN_POINT ( 'NONE',  ( 0.000000000000000000, 0.000000000000000000, 0.000000000000000000 ) ) ;
#63234=DIRECTION ( 'NONE',  ( -1.000000000000000000, 0.000000000000000000, -0.000000000000000000 ) ) ;
#63443=EDGE_CURVE ( 'NONE', #3824, #70051, #23587, .T. ) ;
#63621=ORIENTED_EDGE ( 'NONE', *, *, #13247, .F. ) ;
#64024=CARTESIAN_POINT ( 'NONE',  ( -38.00000000000000000, 63.00000000000000000, 15.00000000000000178 ) ) ;
#64084=DIRECTION ( 'NONE',  ( 0.000000000000000000, -6.938893903907228378E-16, -1.000000000000000000 ) ) ;
#64128=EDGE_CURVE ( 'NONE', #68280, #24567, #65399, .T. ) ;
#64409=ORIENTED_EDGE ( 'NONE', *, *, #64128, .F. ) ;
#64638=VERTEX_POINT ( 'NONE', #7239 ) ;
#64693=ORIENTED_EDGE ( 'NONE', *, *, #10806, .F. ) ;
#64730=ORIENTED_EDGE ( 'NONE', *, *, #16438, .T. ) ;
#65126=AXIS2_PLACEMENT_3D ( 'NONE', #58220, #28776, #35203 ) ;
#65399=LINE ( 'NONE', #36368, #42634 ) ;
#65421=DIRECTION ( 'NONE',  ( -0.000000000000000000, -1.000000000000000000, -0.000000000000000000 ) ) ;
#65593=DIRECTION ( 'NONE',  ( 0.000000000000000000, 1.000000000000000000, -6.938893903907228378E-16 ) ) ;
#65633=DIRECTION ( 'NONE',  ( 0.000000000000000000, 0.000000000000000000, 1.000000000000000000 ) ) ;
#65861=ADVANCED_FACE ( 'NONE', ( #13523 ), #36561, .F. ) ;
#66008=LINE ( 'NONE', #9429, #28674 ) ;
#66021=ORIENTED_EDGE ( 'NONE', *, *, #12860, .F. ) ;
#66228=DIRECTION ( 'NONE',  ( -1.000000000000000000, -0.000000000000000000, -0.000000000000000000 ) ) ;
#66285=PLANE ( 'NONE',  #25455 ) ;
#66347=ORIENTED_EDGE ( 'NONE', *, *, #43219, .T. ) ;
#66373=CARTESIAN_POINT ( 'NONE',  ( -38.00000000000000000, -53.00000000000000711, -5.204170427930421283E-15 ) ) ;
#66518=VECTOR ( 'NONE', #59663, 1000.000000000000000 ) ;
#66659=DIRECTION ( 'NONE',  ( -1.000000000000000000, 0.000000000000000000, -0.000000000000000000 ) ) ;
#67049=PLANE ( 'NONE',  #68110 ) ;
#67088=ORIENTED_EDGE ( 'NONE', *, *, #32302, .F. ) ;
#67429=MANIFOLD_SOLID_BREP ( 'Cut-Extrude1', #70740 ) ;
#67444=LINE ( 'NONE', #68187, #47290 ) ;
#67493=EDGE_LOOP ( 'NONE', ( #20341, #54001, #30773, #71182 ) ) ;
#67516=EDGE_CURVE ( 'NONE', #52559, #40096, #72463, .T. ) ;
#67728=FACE_OUTER_BOUND ( 'NONE', #39618, .T. ) ;
#67737=EDGE_CURVE ( 'NONE', #19664, #5894, #11601, .T. ) ;
#67798=FACE_BOUND ( 'NONE', #67493, .T. ) ;
#67842=PRODUCT_CONTEXT ( 'NONE', #36116, 'mechanical' ) ;
#67900=CARTESIAN_POINT ( 'NONE',  ( 10.99999999999999645, 10.99999999999999645, 25.00000000000000000 ) ) ;
#67950=EDGE_CURVE ( 'NONE', #70051, #19664, #23570, .T. ) ;
#67987=VECTOR ( 'NONE', #770, 1000.000000000000000 ) ;
#68110=AXIS2_PLACEMENT_3D ( 'NONE', #50808, #21756, #61388 ) ;
#68162=CARTESIAN_POINT ( 'NONE',  ( 38.00000000000000000, -52.99999999999999289, 25.00000000000000000 ) ) ;
#68187=CARTESIAN_POINT ( 'NONE',  ( -11.00000000000000000, 11.00000000000000000, -6.938893903907228378E-15 ) ) ;
#68280=VERTEX_POINT ( 'NONE', #1325 ) ;
#68554=DIRECTION ( 'NONE',  ( 1.000000000000000000, 0.000000000000000000, 0.000000000000000000 ) ) ;
#68567=SHAPE_REPRESENTATION ( 'clamping plate', ( #57354 ), #40540 ) ;
#68753=VECTOR ( 'NONE', #66228, 1000.000000000000000 ) ;
#68897=CARTESIAN_POINT ( 'NONE',  ( 38.00000000000000000, 52.99999999999999289, 25.00000000000000000 ) ) ;
#68933=DIRECTION ( 'NONE',  ( -0.000000000000000000, -0.000000000000000000, 1.000000000000000000 ) ) ;
#69368=CARTESIAN_POINT ( 'NONE',  ( -10.99999999999999645, -11.00000000000000000, 25.00000000000000000 ) ) ;
#69467=ADVANCED_FACE ( 'NONE', ( #30911 ), #46781, .F. ) ;
#69496=DIRECTION ( 'NONE',  ( -1.000000000000000000, -0.000000000000000000, -0.000000000000000000 ) ) ;
#69569=DIRECTION ( 'NONE',  ( 0.000000000000000000, 0.000000000000000000, -1.000000000000000000 ) ) ;
#70042=ADVANCED_FACE ( 'NONE', ( #36500 ), #47064, .F. ) ;
#70051=VERTEX_POINT ( 'NONE', #30468 ) ;
#70461=VECTOR ( 'NONE', #50226, 1000.000000000000000 ) ;
#70740=CLOSED_SHELL ( 'NONE', ( #42521, #31562, #65861, #30298, #74263, #10752, #71705, #19712, #70042, #7697, #17494, #15765, #55414, #69467, #7023, #54979 ) ) ;
#70848=CARTESIAN_POINT ( 'NONE',  ( -38.00000000000000000, -52.99999999999999289, 25.00000000000000000 ) ) ;
#70963=EDGE_CURVE ( 'NONE', #41123, #1819, #72118, .T. ) ;
#70965=DIRECTION ( 'NONE',  ( -1.000000000000000000, -0.000000000000000000, -0.000000000000000000 ) ) ;
#71050=DIRECTION ( 'NONE',  ( -1.000000000000000000, -0.000000000000000000, -0.000000000000000000 ) ) ;
#71088=CARTESIAN_POINT ( 'NONE',  ( -11.00000000000000000, 11.00000000000000000, 25.00000000000000000 ) ) ;
#71182=ORIENTED_EDGE ( 'NONE', *, *, #3439, .T. ) ;
#71262=CARTESIAN_POINT ( 'NONE',  ( -10.99999999999999645, -11.00000000000000000, -6.938893903907228378E-15 ) ) ;
#71705=ADVANCED_FACE ( 'NONE', ( #67798, #55744 ), #67049, .F. ) ;
#71708=SHAPE_REPRESENTATION_RELATIONSHIP ( 'NONE' , 'NONE' ,  #68567, #15581 ) ;
#71834=VERTEX_POINT ( 'NONE', #68162 ) ;
#71877=LINE ( 'NONE', #19828, #68753 ) ;
#72118=LINE ( 'NONE', #14771, #58440 ) ;
#72392=CARTESIAN_POINT ( 'NONE',  ( 38.00000000000000000, -52.99999999999999289, 25.00000000000000000 ) ) ;
#72463=LINE ( 'NONE', #53633, #57261 ) ;
#72539=CARTESIAN_POINT ( 'NONE',  ( 38.00000000000000000, -53.00000000000000000, 15.00000000000000178 ) ) ;
#72552=CARTESIAN_POINT ( 'NONE',  ( 38.00000000000000000, 53.00000000000000000, 15.00000000000000178 ) ) ;
#72625=DIRECTION ( 'NONE',  ( 1.000000000000000000, 0.000000000000000000, 0.000000000000000000 ) ) ;
#72639=ORIENTED_EDGE ( 'NONE', *, *, #29419, .F. ) ;
#73041=ORIENTED_EDGE ( 'NONE', *, *, #32608, .F. ) ;
#73102=CARTESIAN_POINT ( 'NONE',  ( -38.00000000000000000, -52.99999999999999289, 25.00000000000000000 ) ) ;
#73162=FACE_OUTER_BOUND ( 'NONE', #50653, .T. ) ;
#73292=ORIENTED_EDGE ( 'NONE', *, *, #57898, .T. ) ;
#73302=AXIS2_PLACEMENT_3D ( 'NONE', #51713, #16247, #27582 ) ;
#73360=CARTESIAN_POINT ( 'NONE',  ( 38.00000000000000000, 53.00000000000000711, 9.999999999999991118 ) ) ;
#73366=EDGE_CURVE ( 'NONE', #3824, #34844, #38018, .T. ) ;
#73576=EDGE_CURVE ( 'NONE', #55047, #45526, #23649, .T. ) ;
#73726=LINE ( 'NONE', #22036, #1363 ) ;
#73897=CARTESIAN_POINT ( 'NONE',  ( -10.99999999999999645, -11.00000000000000000, 25.00000000000000000 ) ) ;
#74263=ADVANCED_FACE ( 'NONE', ( #23549 ), #12228, .F. ) ;
#74267=DIRECTION ( 'NONE',  ( 1.000000000000000000, 0.000000000000000000, 0.000000000000000000 ) ) ;
#74359=CARTESIAN_POINT ( 'NONE',  ( -11.00000000000000000, 11.00000000000000000, 25.00000000000000000 ) ) ;
#74469=PLANE ( 'NONE',  #54389 ) ;
#74470=LINE ( 'NONE', #16739, #14627 ) ;
#74506=ORIENTED_EDGE ( 'NONE', *, *, #23362, .F. ) ;
#74707=COLOUR_RGB('Off White',0.89,0.88,0.83);
#74708=FILL_AREA_STYLE_COLOUR('',#74707);
#74709=FILL_AREA_STYLE('',(#74708));
#74710=SURFACE_STYLE_FILL_AREA(#74709);
#74711=SURFACE_SIDE_STYLE('',(#74710));
#74712=SURFACE_STYLE_USAGE(.BOTH.,#74711);
#74713=PRESENTATION_STYLE_ASSIGNMENT((#74712));
ENDSEC;
END-ISO-10303-21;
